ISO-10303-21;
HEADER;
/* Generated by software containing ST-Developer
 * from STEP Tools, Inc. (www.steptools.com) 
 */

FILE_DESCRIPTION(
/* description */ ('Gravity roller conveyor section'),
/* implementation_level */ '2;1');

FILE_NAME(
/* name */ 'Bonded foot pad (2).step',
/* time_stamp */ '2026-11-02T07:43:02-08:00',
/* author */ (''),
/* organization */ (''),
/* preprocessor_version */ 'ST-DEVELOPER v20.2',
/* originating_system */ 'Autodesk Translation Framework v15.17.0.0',
/* authorisation */ '');

FILE_SCHEMA (('AUTOMOTIVE_DESIGN { 1 0 10303 214 3 1 1 }'));
ENDSEC;

DATA;
#10=MECHANICAL_DESIGN_GEOMETRIC_PRESENTATION_REPRESENTATION('',(#541),#13821);
#473=SHAPE_REPRESENTATION_RELATIONSHIP('SRR','None',#14010,#507);
#507=ADVANCED_BREP_SHAPE_REPRESENTATION('',(#581),#13797);
#541=STYLED_ITEM('',(#14193),#581);
#581=MANIFOLD_SOLID_BREP('Body1',#7641);
#901=PLANE('',#8352);
#902=PLANE('',#8353);
#903=PLANE('',#8354);
#904=PLANE('',#8355);
#905=PLANE('',#8356);
#906=PLANE('',#8357);
#1240=FACE_OUTER_BOUND('',#1700,.T.);
#1241=FACE_OUTER_BOUND('',#1701,.T.);
#1242=FACE_OUTER_BOUND('',#1702,.T.);
#1243=FACE_OUTER_BOUND('',#1703,.T.);
#1244=FACE_OUTER_BOUND('',#1704,.T.);
#1245=FACE_OUTER_BOUND('',#1705,.T.);
#1700=EDGE_LOOP('',(#6414,#6415,#6416,#6417));
#1701=EDGE_LOOP('',(#6418,#6419,#6420,#6421));
#1702=EDGE_LOOP('',(#6422,#6423,#6424,#6425));
#1703=EDGE_LOOP('',(#6426,#6427,#6428,#6429));
#1704=EDGE_LOOP('',(#6430,#6431,#6432,#6433));
#1705=EDGE_LOOP('',(#6434,#6435,#6436,#6437));
#2478=LINE('',#12502,#3196);
#2479=LINE('',#12504,#3197);
#2480=LINE('',#12506,#3198);
#2481=LINE('',#12507,#3199);
#2482=LINE('',#12510,#3200);
#2483=LINE('',#12512,#3201);
#2484=LINE('',#12513,#3202);
#2485=LINE('',#12516,#3203);
#2486=LINE('',#12518,#3204);
#2487=LINE('',#12519,#3205);
#2488=LINE('',#12521,#3206);
#2489=LINE('',#12522,#3207);
#3196=VECTOR('',#9967,1.);
#3197=VECTOR('',#9968,1.);
#3198=VECTOR('',#9969,1.);
#3199=VECTOR('',#9970,1.);
#3200=VECTOR('',#9973,1.);
#3201=VECTOR('',#9974,1.);
#3202=VECTOR('',#9975,1.);
#3203=VECTOR('',#9978,1.);
#3204=VECTOR('',#9979,1.);
#3205=VECTOR('',#9980,1.);
#3206=VECTOR('',#9983,1.);
#3207=VECTOR('',#9984,1.);
#3992=VERTEX_POINT('',#12500);
#3993=VERTEX_POINT('',#12501);
#3994=VERTEX_POINT('',#12503);
#3995=VERTEX_POINT('',#12505);
#3996=VERTEX_POINT('',#12509);
#3997=VERTEX_POINT('',#12511);
#3998=VERTEX_POINT('',#12515);
#3999=VERTEX_POINT('',#12517);
#4844=EDGE_CURVE('',#3992,#3993,#2478,.T.);
#4845=EDGE_CURVE('',#3993,#3994,#2479,.T.);
#4846=EDGE_CURVE('',#3995,#3994,#2480,.T.);
#4847=EDGE_CURVE('',#3992,#3995,#2481,.T.);
#4848=EDGE_CURVE('',#3996,#3992,#2482,.T.);
#4849=EDGE_CURVE('',#3997,#3995,#2483,.T.);
#4850=EDGE_CURVE('',#3996,#3997,#2484,.T.);
#4851=EDGE_CURVE('',#3998,#3996,#2485,.T.);
#4852=EDGE_CURVE('',#3999,#3997,#2486,.T.);
#4853=EDGE_CURVE('',#3998,#3999,#2487,.T.);
#4854=EDGE_CURVE('',#3993,#3998,#2488,.T.);
#4855=EDGE_CURVE('',#3994,#3999,#2489,.T.);
#6414=ORIENTED_EDGE('',*,*,#4844,.T.);
#6415=ORIENTED_EDGE('',*,*,#4845,.T.);
#6416=ORIENTED_EDGE('',*,*,#4846,.F.);
#6417=ORIENTED_EDGE('',*,*,#4847,.F.);
#6418=ORIENTED_EDGE('',*,*,#4848,.T.);
#6419=ORIENTED_EDGE('',*,*,#4847,.T.);
#6420=ORIENTED_EDGE('',*,*,#4849,.F.);
#6421=ORIENTED_EDGE('',*,*,#4850,.F.);
#6422=ORIENTED_EDGE('',*,*,#4851,.T.);
#6423=ORIENTED_EDGE('',*,*,#4850,.T.);
#6424=ORIENTED_EDGE('',*,*,#4852,.F.);
#6425=ORIENTED_EDGE('',*,*,#4853,.F.);
#6426=ORIENTED_EDGE('',*,*,#4854,.T.);
#6427=ORIENTED_EDGE('',*,*,#4853,.T.);
#6428=ORIENTED_EDGE('',*,*,#4855,.F.);
#6429=ORIENTED_EDGE('',*,*,#4845,.F.);
#6430=ORIENTED_EDGE('',*,*,#4855,.T.);
#6431=ORIENTED_EDGE('',*,*,#4852,.T.);
#6432=ORIENTED_EDGE('',*,*,#4849,.T.);
#6433=ORIENTED_EDGE('',*,*,#4846,.T.);
#6434=ORIENTED_EDGE('',*,*,#4854,.F.);
#6435=ORIENTED_EDGE('',*,*,#4844,.F.);
#6436=ORIENTED_EDGE('',*,*,#4848,.F.);
#6437=ORIENTED_EDGE('',*,*,#4851,.F.);
#7441=ADVANCED_FACE('',(#1240),#901,.T.);
#7442=ADVANCED_FACE('',(#1241),#902,.T.);
#7443=ADVANCED_FACE('',(#1242),#903,.T.);
#7444=ADVANCED_FACE('',(#1243),#904,.T.);
#7445=ADVANCED_FACE('',(#1244),#905,.T.);
#7446=ADVANCED_FACE('',(#1245),#906,.F.);
#7641=CLOSED_SHELL('',(#7441,#7442,#7443,#7444,#7445,#7446));
#8351=AXIS2_PLACEMENT_3D('',#12498,#9963,#9964);
#8352=AXIS2_PLACEMENT_3D('',#12499,#9965,#9966);
#8353=AXIS2_PLACEMENT_3D('',#12508,#9971,#9972);
#8354=AXIS2_PLACEMENT_3D('',#12514,#9976,#9977);
#8355=AXIS2_PLACEMENT_3D('',#12520,#9981,#9982);
#8356=AXIS2_PLACEMENT_3D('',#12523,#9985,#9986);
#8357=AXIS2_PLACEMENT_3D('',#12524,#9987,#9988);
#9963=DIRECTION('axis',(0.,0.,1.));
#9964=DIRECTION('refdir',(1.,0.,0.));
#9965=DIRECTION('center_axis',(0.,1.,0.));
#9966=DIRECTION('ref_axis',(-1.,0.,0.));
#9967=DIRECTION('',(-1.,0.,0.));
#9968=DIRECTION('',(0.,0.,1.));
#9969=DIRECTION('',(-1.,0.,0.));
#9970=DIRECTION('',(0.,0.,1.));
#9971=DIRECTION('center_axis',(1.,0.,0.));
#9972=DIRECTION('ref_axis',(0.,1.,0.));
#9973=DIRECTION('',(0.,1.,0.));
#9974=DIRECTION('',(0.,1.,0.));
#9975=DIRECTION('',(0.,0.,1.));
#9976=DIRECTION('center_axis',(0.,-1.,0.));
#9977=DIRECTION('ref_axis',(1.,0.,0.));
#9978=DIRECTION('',(1.,0.,0.));
#9979=DIRECTION('',(1.,0.,0.));
#9980=DIRECTION('',(0.,0.,1.));
#9981=DIRECTION('center_axis',(-1.,0.,0.));
#9982=DIRECTION('ref_axis',(0.,-1.,0.));
#9983=DIRECTION('',(0.,-1.,0.));
#9984=DIRECTION('',(0.,-1.,0.));
#9985=DIRECTION('center_axis',(0.,0.,1.));
#9986=DIRECTION('ref_axis',(1.,0.,0.));
#9987=DIRECTION('center_axis',(0.,0.,1.));
#9988=DIRECTION('ref_axis',(1.,0.,0.));
#12498=CARTESIAN_POINT('',(0.,0.,0.));
#12499=CARTESIAN_POINT('Origin',(56.,-3.5,-17.6));
#12500=CARTESIAN_POINT('',(56.,-3.5,-17.6));
#12501=CARTESIAN_POINT('',(52.,-3.5,-17.6));
#12502=CARTESIAN_POINT('',(56.,-3.5,-17.6));
#12503=CARTESIAN_POINT('',(52.,-3.5,-16.8));
#12504=CARTESIAN_POINT('',(52.,-3.5,-17.6));
#12505=CARTESIAN_POINT('',(56.,-3.5,-16.8));
#12506=CARTESIAN_POINT('',(56.,-3.5,-16.8));
#12507=CARTESIAN_POINT('',(56.,-3.5,-17.6));
#12508=CARTESIAN_POINT('Origin',(56.,-5.,-17.6));
#12509=CARTESIAN_POINT('',(56.,-5.,-17.6));
#12510=CARTESIAN_POINT('',(56.,-5.,-17.6));
#12511=CARTESIAN_POINT('',(56.,-5.,-16.8));
#12512=CARTESIAN_POINT('',(56.,-5.,-16.8));
#12513=CARTESIAN_POINT('',(56.,-5.,-17.6));
#12514=CARTESIAN_POINT('Origin',(52.,-5.,-17.6));
#12515=CARTESIAN_POINT('',(52.,-5.,-17.6));
#12516=CARTESIAN_POINT('',(52.,-5.,-17.6));
#12517=CARTESIAN_POINT('',(52.,-5.,-16.8));
#12518=CARTESIAN_POINT('',(52.,-5.,-16.8));
#12519=CARTESIAN_POINT('',(52.,-5.,-17.6));
#12520=CARTESIAN_POINT('Origin',(52.,-3.5,-17.6));
#12521=CARTESIAN_POINT('',(52.,-3.5,-17.6));
#12522=CARTESIAN_POINT('',(52.,-3.5,-16.8));
#12523=CARTESIAN_POINT('Origin',(54.,-4.25,-16.8));
#12524=CARTESIAN_POINT('Origin',(54.,-4.25,-17.6));
#13758=UNCERTAINTY_MEASURE_WITH_UNIT(LENGTH_MEASURE(0.001),#13822,
'DISTANCE_ACCURACY_VALUE',
'Maximum model space distance between geometric entities at asserted c
onnectivities');
#13782=UNCERTAINTY_MEASURE_WITH_UNIT(LENGTH_MEASURE(0.001),#13822,
'DISTANCE_ACCURACY_VALUE',
'Maximum model space distance between geometric entities at asserted c
onnectivities');
#13797=(
GEOMETRIC_REPRESENTATION_CONTEXT(3)
GLOBAL_UNCERTAINTY_ASSIGNED_CONTEXT((#13758))
GLOBAL_UNIT_ASSIGNED_CONTEXT((#13822,#13824,#13825))
REPRESENTATION_CONTEXT('','3D')
);
#13821=(
GEOMETRIC_REPRESENTATION_CONTEXT(3)
GLOBAL_UNCERTAINTY_ASSIGNED_CONTEXT((#13782))
GLOBAL_UNIT_ASSIGNED_CONTEXT((#13822,#13824,#13825))
REPRESENTATION_CONTEXT('','3D')
);
#13822=(
LENGTH_UNIT()
NAMED_UNIT(*)
SI_UNIT(.CENTI.,.METRE.)
);
#13824=(
NAMED_UNIT(*)
PLANE_ANGLE_UNIT()
SI_UNIT($,.RADIAN.)
);
#13825=(
NAMED_UNIT(*)
SI_UNIT($,.STERADIAN.)
SOLID_ANGLE_UNIT()
);
#13840=SHAPE_DEFINITION_REPRESENTATION(#13878,#14010);
#13878=PRODUCT_DEFINITION_SHAPE('',$,#14049);
#14010=SHAPE_REPRESENTATION('',(#8351),#13797);
#14034=PRODUCT_DEFINITION_CONTEXT('part definition',#14150,'design');
#14049=PRODUCT_DEFINITION('Bonded foot pad_2','Bonded foot pad (2)',#14087,
#14034);
#14087=PRODUCT_DEFINITION_FORMATION('',$,#14166);
#14150=APPLICATION_CONTEXT(
'Core Data for Automotive Mechanical Design Process');
#14151=PRODUCT_CONTEXT('part definition',#14150,'mechanical');
#14166=PRODUCT('Bonded foot pad_2','Bonded foot pad (2)',
'Bonded foot pad',(#14151));
#14193=PRESENTATION_STYLE_ASSIGNMENT((#14198));
#14198=SURFACE_STYLE_USAGE(.BOTH.,#14203);
#14203=SURFACE_SIDE_STYLE('',(#14208));
#14208=SURFACE_STYLE_FILL_AREA(#14213);
#14213=FILL_AREA_STYLE('CAD Library Painted - Graphite',(#14218));
#14218=FILL_AREA_STYLE_COLOUR('CAD Library Painted - Graphite',#14223);
#14223=COLOUR_RGB('CAD Library Painted - Graphite',0.168627450980392,0.192156862745098,
0.231372549019608);
ENDSEC;
END-ISO-10303-21;
